ISO-10303-21;
HEADER;
FILE_DESCRIPTION (('STEP AP214'),
    '1' );
FILE_NAME ('socket head cap screw_iso_ISO 4762 M3 x 8 - 8N.step',
    '2026-10-08T14:41:38',
    ( '' ),
    ( '' ),
    'SwSTEP 2.0',
    'SolidWorks 2026',
    '' );
FILE_SCHEMA (( 'AUTOMOTIVE_DESIGN' ));
ENDSEC;

DATA;
#37=DIRECTION ( 'NONE',  ( -1.000000000000000000, -0.000000000000000000, -0.000000000000000000 ) ) ;
#95=ORIENTED_EDGE ( 'NONE', *, *, #5527, .F. ) ;
#96=EDGE_LOOP ( 'NONE', ( #12565, #3709, #10938 ) ) ;
#118=DIRECTION ( 'NONE',  ( -1.000000000000000000, -0.000000000000000000, -0.000000000000000000 ) ) ;
#128=ORIENTED_EDGE ( 'NONE', *, *, #13504, .F. ) ;
#201=VERTEX_POINT ( 'NONE', #6735 ) ;
#238=DIRECTION ( 'NONE',  ( 0.000000000000000000, -0.4999999999999992784, 0.8660254037844390407 ) ) ;
#259=EDGE_CURVE ( 'NONE', #2631, #2004, #1460, .T. ) ;
#260=PLANE ( 'NONE',  #8615 ) ;
#262=VERTEX_POINT ( 'NONE', #4895 ) ;
#282=CARTESIAN_POINT ( 'NONE',  ( 1.300000000000000044, 0.7390083445627193548, -1.280000000000000693 ) ) ;
#306=( NAMED_UNIT ( * ) PLANE_ANGLE_UNIT ( ) SI_UNIT ( $, .RADIAN. ) );
#317=DIRECTION ( 'NONE',  ( 0.000000000000000000, 0.000000000000000000, 1.000000000000000000 ) ) ;
#418=ADVANCED_FACE ( 'NONE', ( #11608 ), #4181, .T. ) ;
#484=PRODUCT_DEFINITION_FORMATION_WITH_SPECIFIED_SOURCE ( 'ANY', '', #8955, .NOT_KNOWN. ) ;
#502=AXIS2_PLACEMENT_3D ( 'NONE', #7049, #17444, #4014 ) ;
#503=LINE ( 'NONE', #18262, #13813 ) ;
#504=CIRCLE ( 'NONE', #4888, 1.280000000000000027 ) ;
#541=CYLINDRICAL_SURFACE ( 'NONE', #12959, 2.750000000000000000 ) ;
#570=FACE_OUTER_BOUND ( 'NONE', #5222, .T. ) ;
#613=DIRECTION ( 'NONE',  ( 1.000000000000000000, 0.000000000000000000, 0.000000000000000000 ) ) ;
#688=DIRECTION ( 'NONE',  ( 0.000000000000000000, 0.4999999999999991673, -0.8660254037844391517 ) ) ;
#718=LINE ( 'NONE', #13034, #5625 ) ;
#723=CARTESIAN_POINT ( 'NONE',  ( 1.300000000000000044, -1.478016689125442706, 1.843143693225357538E-15 ) ) ;
#751=FACE_OUTER_BOUND ( 'NONE', #949, .T. ) ;
#777=ORIENTED_EDGE ( 'NONE', *, *, #13586, .F. ) ;
#806=DIRECTION ( 'NONE',  ( 1.000000000000000000, 0.000000000000000000, 0.000000000000000000 ) ) ;
#823=FACE_OUTER_BOUND ( 'NONE', #4002, .T. ) ;
#834=VERTEX_POINT ( 'NONE', #18496 ) ;
#867=EDGE_CURVE ( 'NONE', #15167, #11814, #11394, .T. ) ;
#919=DIRECTION ( 'NONE',  ( -0.000000000000000000, 1.000000000000000000, 1.224646799147353207E-16 ) ) ;
#949=EDGE_LOOP ( 'NONE', ( #17084, #14289, #6599, #2912 ) ) ;
#965=EDGE_CURVE ( 'NONE', #11814, #8458, #14994, .T. ) ;
#973=DIRECTION ( 'NONE',  ( -1.000000000000000000, -0.000000000000000000, -0.000000000000000000 ) ) ;
#1015=EDGE_LOOP ( 'NONE', ( #19019, #777, #10744, #12366, #12548 ) ) ;
#1024=EDGE_CURVE ( 'NONE', #2345, #11043, #14353, .T. ) ;
#1030=EDGE_LOOP ( 'NONE', ( #12141, #15928, #19063, #7063 ) ) ;
#1039=EDGE_CURVE ( 'NONE', #11212, #11751, #10602, .T. ) ;
#1043=DIRECTION ( 'NONE',  ( 1.000000000000000000, 0.000000000000000000, 0.000000000000000000 ) ) ;
#1046=ORIENTED_EDGE ( 'NONE', *, *, #14507, .T. ) ;
#1056=FACE_OUTER_BOUND ( 'NONE', #18608, .T. ) ;
#1062=EDGE_LOOP ( 'NONE', ( #3805, #13532, #11853, #1160 ) ) ;
#1064=ADVANCED_FACE ( 'NONE', ( #17779 ), #1535, .T. ) ;
#1105=ORIENTED_EDGE ( 'NONE', *, *, #7076, .F. ) ;
#1122=EDGE_LOOP ( 'NONE', ( #4526, #1404, #11624, #13740, #11083 ) ) ;
#1123=( NAMED_UNIT ( * ) PLANE_ANGLE_UNIT ( ) SI_UNIT ( $, .RADIAN. ) );
#1138=DIRECTION ( 'NONE',  ( 0.000000000000000000, 0.000000000000000000, -1.000000000000000000 ) ) ;
#1150=EDGE_CURVE ( 'NONE', #262, #14577, #1861, .T. ) ;
#1155=DIRECTION ( 'NONE',  ( 0.000000000000000000, -0.4999999999999991118, 0.8660254037844391517 ) ) ;
#1156=ORIENTED_EDGE ( 'NONE', *, *, #5431, .F. ) ;
#1160=ORIENTED_EDGE ( 'NONE', *, *, #1024, .F. ) ;
#1179=EDGE_LOOP ( 'NONE', ( #8689, #16157, #9561, #9596, #14121, #1902 ) ) ;
#1199=DIRECTION ( 'NONE',  ( 0.000000000000000000, 0.000000000000000000, 1.000000000000000000 ) ) ;
#1206=DIRECTION ( 'NONE',  ( -1.000000000000000000, -0.000000000000000000, -0.000000000000000000 ) ) ;
#1211=AXIS2_PLACEMENT_3D ( 'NONE', #13801, #15278, #3324 ) ;
#1230=CIRCLE ( 'NONE', #7825, 1.280000000000000027 ) ;
#1270=CIRCLE ( 'NONE', #18792, 2.750000000000000000 ) ;
#1277=AXIS2_PLACEMENT_3D ( 'NONE', #7864, #13727, #3147 ) ;
#1288=DIRECTION ( 'NONE',  ( 0.000000000000000000, -0.4999999999999992784, 0.8660254037844390407 ) ) ;
#1318=DIRECTION ( 'NONE',  ( 0.000000000000000000, 0.000000000000000000, 1.000000000000000000 ) ) ;
#1327=FILL_AREA_STYLE ('',( #8960 ) ) ;
#1404=ORIENTED_EDGE ( 'NONE', *, *, #7566, .F. ) ;
#1409=LINE ( 'NONE', #10410, #12032 ) ;
#1419=( GEOMETRIC_REPRESENTATION_CONTEXT ( 3 ) GLOBAL_UNCERTAINTY_ASSIGNED_CONTEXT ( ( #16497 ) ) GLOBAL_UNIT_ASSIGNED_CONTEXT ( ( #13368, #7102, #10323 ) ) REPRESENTATION_CONTEXT ( 'NONE', 'WORKASPACE' ) );
#1460=LINE ( 'NONE', #14092, #6627 ) ;
#1500=EDGE_CURVE ( 'NONE', #6864, #2345, #4009, .T. ) ;
#1507=CARTESIAN_POINT ( 'NONE',  ( 1.300000000000000044, 1.478016689125442484, -1.626303258728256651E-15 ) ) ;
#1535=TOROIDAL_SURFACE ( 'NONE', #3092, 2.600000000000000089, 0.1499999999999999944 ) ;
#1543=CIRCLE ( 'NONE', #1211, 2.750000000000000000 ) ;
#1560=AXIS2_PLACEMENT_3D ( 'NONE', #5311, #3743, #6869 ) ;
#1593=AXIS2_PLACEMENT_3D ( 'NONE', #11491, #17887, #16509 ) ;
#1601=UNCERTAINTY_MEASURE_WITH_UNIT (LENGTH_MEASURE( 1.000000000000000082E-05 ), #14848, 'distance_accuracy_value', 'NONE');
#1610=ORIENTED_EDGE ( 'NONE', *, *, #3289, .F. ) ;
#1615=LINE ( 'NONE', #12083, #12230 ) ;
#1625=STYLED_ITEM ( 'NONE', ( #9316 ), #10426 ) ;
#1644=CARTESIAN_POINT ( 'NONE',  ( 1.300000000000000044, -0.7390083445627200209, 1.280000000000001137 ) ) ;
#1748=ORIENTED_EDGE ( 'NONE', *, *, #13669, .T. ) ;
#1758=CIRCLE ( 'NONE', #5827, 1.500000000000000222 ) ;
#1791=AXIS2_PLACEMENT_3D ( 'NONE', #13713, #4815, #7646 ) ;
#1800=EDGE_LOOP ( 'NONE', ( #4603, #7930, #11547 ) ) ;
#1861=CIRCLE ( 'NONE', #4364, 0.1499999999999999667 ) ;
#1869=EDGE_LOOP ( 'NONE', ( #14388, #8355 ) ) ;
#1875=SURFACE_STYLE_FILL_AREA ( #16684 ) ;
#1902=ORIENTED_EDGE ( 'NONE', *, *, #8070, .F. ) ;
#1919=EDGE_CURVE ( 'NONE', #7133, #14697, #1230, .T. ) ;
#1932=CARTESIAN_POINT ( 'NONE',  ( 3.000000000000000000, 0.000000000000000000, -1.600000000000000311 ) ) ;
#1969=EDGE_CURVE ( 'NONE', #17858, #7133, #10591, .T. ) ;
#1977=CARTESIAN_POINT ( 'NONE',  ( 0.000000000000000000, 0.000000000000000000, 0.000000000000000000 ) ) ;
#2004=VERTEX_POINT ( 'NONE', #9942 ) ;
#2048=TOROIDAL_SURFACE ( 'NONE', #502, 2.600000000000000089, 0.1499999999999999944 ) ;
#2163=CIRCLE ( 'NONE', #9081, 2.600000000000000089 ) ;
#2164=DIRECTION ( 'NONE',  ( 0.000000000000000000, -0.5000000000000009992, -0.8660254037844380415 ) ) ;
#2176=VECTOR ( 'NONE', #9853, 1000.000000000000000 ) ;
#2234=MECHANICAL_DESIGN_GEOMETRIC_PRESENTATION_REPRESENTATION('',(#1625),#17896);
#2242=VECTOR ( 'NONE', #5458, 1000.000000000000227 ) ;
#2260=ADVANCED_FACE ( 'NONE', ( #12105 ), #9336, .F. ) ;
#2325=CARTESIAN_POINT ( 'NONE',  ( 1.300000000000000044, 1.478016689125442484, -1.626303258728256651E-15 ) ) ;
#2345=VERTEX_POINT ( 'NONE', #9359 ) ;
#2395=LINE ( 'NONE', #8380, #8279 ) ;
#2421=EDGE_LOOP ( 'NONE', ( #16978, #6316, #18315, #9665 ) ) ;
#2480=VECTOR ( 'NONE', #2940, 1000.000000000000227 ) ;
#2494=CIRCLE ( 'NONE', #16609, 1.219500000000000028 ) ;
#2499=VECTOR ( 'NONE', #1288, 1000.000000000000000 ) ;
#2534=CARTESIAN_POINT ( 'NONE',  ( 3.000000000000000000, 1.959434878635765477E-16, 1.600000000000000311 ) ) ;
#2606=ORIENTED_EDGE ( 'NONE', *, *, #1150, .T. ) ;
#2631=VERTEX_POINT ( 'NONE', #9536 ) ;
#2679=APPLICATION_CONTEXT ( 'automotive_design' ) ;
#2702=DIRECTION ( 'NONE',  ( -1.000000000000000000, -0.000000000000000000, -0.000000000000000000 ) ) ;
#2731=DIRECTION ( 'NONE',  ( -0.7071067811865335839, 8.659560562355102956E-17, -0.7071067811865614505 ) ) ;
#2805=DIRECTION ( 'NONE',  ( 0.000000000000000000, 0.000000000000000000, -1.000000000000000000 ) ) ;
#2827=CONICAL_SURFACE ( 'NONE', #3142, 1.219500000000000028, 0.7853981633974680410 ) ;
#2838=CIRCLE ( 'NONE', #1593, 2.750000000000000000 ) ;
#2888=PRESENTATION_STYLE_ASSIGNMENT (( #10032 ) ) ;
#2905=EDGE_CURVE ( 'NONE', #13286, #2004, #9310, .T. ) ;
#2912=ORIENTED_EDGE ( 'NONE', *, *, #12038, .T. ) ;
#2940=DIRECTION ( 'NONE',  ( 0.000000000000000000, -0.5000000000000013323, -0.8660254037844378194 ) ) ;
#2945=EDGE_LOOP ( 'NONE', ( #9798, #14980, #7780, #17743, #13882 ) ) ;
#3034=ORIENTED_EDGE ( 'NONE', *, *, #1039, .F. ) ;
#3072=DIRECTION ( 'NONE',  ( 0.000000000000000000, 1.000000000000000000, -1.224646799147353207E-16 ) ) ;
#3092=AXIS2_PLACEMENT_3D ( 'NONE', #7588, #13453, #10114 ) ;
#3142=AXIS2_PLACEMENT_3D ( 'NONE', #15308, #11169, #5024 ) ;
#3147=DIRECTION ( 'NONE',  ( 0.000000000000000000, 0.000000000000000000, 1.000000000000000000 ) ) ;
#3172=CARTESIAN_POINT ( 'NONE',  ( 1.300000000000000044, 1.478016689125442484, -1.626303258728256651E-15 ) ) ;
#3197=ADVANCED_FACE ( 'NONE', ( #1056 ), #14296, .T. ) ;
#3216=DIRECTION ( 'NONE',  ( -1.000000000000000000, -0.000000000000000000, -0.000000000000000000 ) ) ;
#3282=ORIENTED_EDGE ( 'NONE', *, *, #7108, .T. ) ;
#3285=VECTOR ( 'NONE', #5821, 1000.000000000000000 ) ;
#3289=EDGE_CURVE ( 'NONE', #14577, #8458, #13150, .T. ) ;
#3310=EDGE_CURVE ( 'NONE', #15535, #15167, #1270, .T. ) ;
#3321=LINE ( 'NONE', #15087, #14393 ) ;
#3324=DIRECTION ( 'NONE',  ( 0.000000000000000000, 0.000000000000000000, 1.000000000000000000 ) ) ;
#3351=FILL_AREA_STYLE_COLOUR ( '', #16640 ) ;
#3417=AXIS2_PLACEMENT_3D ( 'NONE', #12133, #8901, #4206 ) ;
#3426=EDGE_LOOP ( 'NONE', ( #5112, #12435, #9961, #10168 ) ) ;
#3437=DIRECTION ( 'NONE',  ( 0.000000000000000000, 1.000000000000000000, -1.320393690296331133E-15 ) ) ;
#3439=DIRECTION ( 'NONE',  ( 0.000000000000000000, 1.000000000000000000, -1.320393690296331133E-15 ) ) ;
#3524=EDGE_CURVE ( 'NONE', #12231, #11212, #6213, .T. ) ;
#3568=UNCERTAINTY_MEASURE_WITH_UNIT (LENGTH_MEASURE( 1.000000000000000082E-05 ), #7762, 'distance_accuracy_value', 'NONE');
#3601=( GEOMETRIC_REPRESENTATION_CONTEXT ( 3 ) GLOBAL_UNCERTAINTY_ASSIGNED_CONTEXT ( ( #1601 ) ) GLOBAL_UNIT_ASSIGNED_CONTEXT ( ( #14848, #1123, #5737 ) ) REPRESENTATION_CONTEXT ( 'NONE', 'WORKASPACE' ) );
#3602=CARTESIAN_POINT ( 'NONE',  ( -31.74999999999995737, 0.000000000000000000, 0.000000000000000000 ) ) ;
#3609=DIRECTION ( 'NONE',  ( -1.000000000000000000, 0.000000000000000000, -0.000000000000000000 ) ) ;
#3647=EDGE_LOOP ( 'NONE', ( #17612, #18444, #16454 ) ) ;
#3700=DIRECTION ( 'NONE',  ( 1.000000000000000000, 0.000000000000000000, 0.000000000000000000 ) ) ;
#3709=ORIENTED_EDGE ( 'NONE', *, *, #13504, .T. ) ;
#3724=DIRECTION ( 'NONE',  ( 0.000000000000000000, 0.000000000000000000, 1.000000000000000000 ) ) ;
#3743=DIRECTION ( 'NONE',  ( -0.000000000000000000, 1.320393690296331133E-15, 1.000000000000000000 ) ) ;
#3805=ORIENTED_EDGE ( 'NONE', *, *, #1500, .F. ) ;
#3831=FACE_OUTER_BOUND ( 'NONE', #10868, .T. ) ;
#3872=ORIENTED_EDGE ( 'NONE', *, *, #1500, .T. ) ;
#3885=CARTESIAN_POINT ( 'NONE',  ( 1.300000000000000044, -0.7390083445627200209, 1.280000000000001137 ) ) ;
#3893=ORIENTED_EDGE ( 'NONE', *, *, #3310, .F. ) ;
#3938=FACE_OUTER_BOUND ( 'NONE', #1869, .T. ) ;
#4002=EDGE_LOOP ( 'NONE', ( #10750, #10946, #7542, #17967 ) ) ;
#4009=LINE ( 'NONE', #9882, #11875 ) ;
#4014=DIRECTION ( 'NONE',  ( 0.000000000000000000, 0.000000000000000000, 1.000000000000000000 ) ) ;
#4077=VECTOR ( 'NONE', #15130, 1000.000000000000000 ) ;
#4111=CARTESIAN_POINT ( 'NONE',  ( -31.74999999999995737, 1.836970198721030181E-16, -1.500000000000000222 ) ) ;
#4149=DIRECTION ( 'NONE',  ( 1.000000000000000000, 0.000000000000000000, 0.000000000000000000 ) ) ;
#4173=SHAPE_REPRESENTATION_RELATIONSHIP ( 'NONE' , 'NONE' ,  #8522, #6657 ) ;
#4181=CYLINDRICAL_SURFACE ( 'NONE', #5374, 2.750000000000000000 ) ;
#4182=DIRECTION ( 'NONE',  ( -0.7071067811865335839, 0.000000000000000000, 0.7071067811865614505 ) ) ;
#4206=DIRECTION ( 'NONE',  ( 0.000000000000000000, 0.000000000000000000, -1.000000000000000000 ) ) ;
#4214=EDGE_LOOP ( 'NONE', ( #9867, #9681 ) ) ;
#4318=ORIENTED_EDGE ( 'NONE', *, *, #18246, .T. ) ;
#4352=CARTESIAN_POINT ( 'NONE',  ( 1.300000000000000044, -0.7390083445627225744, -1.279999999999999138 ) ) ;
#4364=AXIS2_PLACEMENT_3D ( 'NONE', #14840, #19352, #17886 ) ;
#4380=DIRECTION ( 'NONE',  ( 0.000000000000000000, 0.000000000000000000, 1.000000000000000000 ) ) ;
#4383=AXIS2_PLACEMENT_3D ( 'NONE', #11244, #7035, #1155 ) ;
#4442=FACE_OUTER_BOUND ( 'NONE', #10258, .T. ) ;
#4464=CARTESIAN_POINT ( 'NONE',  ( 0.000000000000000000, 1.478016689125442484, -1.626303258728256651E-15 ) ) ;
#4473=EDGE_CURVE ( 'NONE', #6864, #201, #2494, .T. ) ;
#4481=DIRECTION ( 'NONE',  ( -1.000000000000000000, -0.000000000000000000, -0.000000000000000000 ) ) ;
#4494=EDGE_LOOP ( 'NONE', ( #16084, #8632, #3034 ) ) ;
#4526=ORIENTED_EDGE ( 'NONE', *, *, #16826, .F. ) ;
#4533=EDGE_CURVE ( 'NONE', #11043, #6946, #3321, .T. ) ;
#4582=ADVANCED_FACE ( 'NONE', ( #751 ), #6921, .T. ) ;
#4603=ORIENTED_EDGE ( 'NONE', *, *, #9391, .T. ) ;
#4635=EDGE_CURVE ( 'NONE', #18570, #15994, #7013, .T. ) ;
#4668=DIRECTION ( 'NONE',  ( -1.000000000000000000, -0.000000000000000000, -0.000000000000000000 ) ) ;
#4809=FACE_BOUND ( 'NONE', #1179, .T. ) ;
#4815=DIRECTION ( 'NONE',  ( 0.000000000000000000, 0.000000000000000000, 1.000000000000000000 ) ) ;
#4888=AXIS2_PLACEMENT_3D ( 'NONE', #7728, #3216, #15176 ) ;
#4895=CARTESIAN_POINT ( 'NONE',  ( 0.1499999999999973577, 0.000000000000000000, 2.750000000000000000 ) ) ;
#4899=CARTESIAN_POINT ( 'NONE',  ( 1.300000000000000044, 1.478016689125442484, -1.626303258728256651E-15 ) ) ;
#4916=VERTEX_POINT ( 'NONE', #16206 ) ;
#4918=AXIS2_PLACEMENT_3D ( 'NONE', #7468, #10200, #18068 ) ;
#4931=FACE_OUTER_BOUND ( 'NONE', #1062, .T. ) ;
#4950=FACE_OUTER_BOUND ( 'NONE', #13209, .T. ) ;
#4952=ADVANCED_FACE ( 'NONE', ( #16877 ), #6680, .F. ) ;
#4989=EDGE_CURVE ( 'NONE', #8458, #14577, #2163, .T. ) ;
#4997=VECTOR ( 'NONE', #14685, 1000.000000000000114 ) ;
#5024=DIRECTION ( 'NONE',  ( 0.000000000000000000, 0.000000000000000000, 1.000000000000000000 ) ) ;
#5047=DIRECTION ( 'NONE',  ( 0.000000000000000000, 0.000000000000000000, -1.000000000000000000 ) ) ;
#5062=CLOSED_SHELL ( 'NONE', ( #2260, #1064, #5346, #15951, #8191, #418, #9634, #13208, #7215, #4582, #9004, #6522, #13750, #17485, #11180, #5784, #14930, #3197, #6379, #4952, #8175, #7414, #8034, #18742, #18530, #9725, #5556 ) ) ;
#5090=DIRECTION ( 'NONE',  ( 0.000000000000000000, 0.000000000000000000, 1.000000000000000000 ) ) ;
#5112=ORIENTED_EDGE ( 'NONE', *, *, #12038, .F. ) ;
#5141=FACE_OUTER_BOUND ( 'NONE', #2421, .T. ) ;
#5190=EDGE_LOOP ( 'NONE', ( #3893, #1156 ) ) ;
#5201=EDGE_CURVE ( 'NONE', #2345, #16414, #15876, .T. ) ;
#5219=ORIENTED_EDGE ( 'NONE', *, *, #7105, .F. ) ;
#5222=EDGE_LOOP ( 'NONE', ( #18536, #8538 ) ) ;
#5277=ORIENTED_EDGE ( 'NONE', *, *, #9391, .F. ) ;
#5311=CARTESIAN_POINT ( 'NONE',  ( 1.300000000000000044, -0.7390083445627200209, 1.280000000000001137 ) ) ;
#5346=ADVANCED_FACE ( 'NONE', ( #16361 ), #13743, .F. ) ;
#5374=AXIS2_PLACEMENT_3D ( 'NONE', #16130, #17228, #17604 ) ;
#5380=ORIENTED_EDGE ( 'NONE', *, *, #4533, .F. ) ;
#5392=EDGE_CURVE ( 'NONE', #7133, #15771, #6171, .T. ) ;
#5431=EDGE_CURVE ( 'NONE', #15167, #15535, #1543, .T. ) ;
#5457=DIRECTION ( 'NONE',  ( 0.000000000000000000, 0.000000000000000000, 1.000000000000000000 ) ) ;
#5458=DIRECTION ( 'NONE',  ( 0.000000000000000000, -0.5000000000000013323, -0.8660254037844378194 ) ) ;
#5459=PLANE ( 'NONE',  #5655 ) ;
#5527=EDGE_CURVE ( 'NONE', #14697, #18570, #17321, .T. ) ;
#5556=ADVANCED_FACE ( 'NONE', ( #11610 ), #12492, .F. ) ;
#5625=VECTOR ( 'NONE', #18935, 1000.000000000000114 ) ;
#5636=EDGE_LOOP ( 'NONE', ( #13367, #3282, #1046, #15658, #6962 ) ) ;
#5655=AXIS2_PLACEMENT_3D ( 'NONE', #2325, #1043, #14663 ) ;
#5667=FACE_OUTER_BOUND ( 'NONE', #1122, .T. ) ;
#5674=EDGE_CURVE ( 'NONE', #201, #11043, #12003, .T. ) ;
#5737=( NAMED_UNIT ( * ) SI_UNIT ( $, .STERADIAN. ) SOLID_ANGLE_UNIT ( ) );
#5782=DIRECTION ( 'NONE',  ( -1.000000000000000000, -0.000000000000000000, -0.000000000000000000 ) ) ;
#5784=ADVANCED_FACE ( 'NONE', ( #14414 ), #11461, .F. ) ;
#5821=DIRECTION ( 'NONE',  ( 0.000000000000000000, -1.000000000000000000, 1.026972870230479989E-15 ) ) ;
#5827=AXIS2_PLACEMENT_3D ( 'NONE', #14664, #14867, #2805 ) ;
#5840=AXIS2_PLACEMENT_3D ( 'NONE', #6516, #14242, #5047 ) ;
#5894=CARTESIAN_POINT ( 'NONE',  ( 1.300000000000000044, -0.7390083445627200209, 1.280000000000001137 ) ) ;
#5919=PLANE ( 'NONE',  #18193 ) ;
#5937=EDGE_CURVE ( 'NONE', #12231, #11751, #19124, .T. ) ;
#6099=LINE ( 'NONE', #10493, #8490 ) ;
#6171=LINE ( 'NONE', #8999, #4997 ) ;
#6178=DIRECTION ( 'NONE',  ( 0.000000000000000000, 0.000000000000000000, 1.000000000000000000 ) ) ;
#6213=LINE ( 'NONE', #1507, #4077 ) ;
#6216=VERTEX_POINT ( 'NONE', #4352 ) ;
#6267=FACE_OUTER_BOUND ( 'NONE', #3647, .T. ) ;
#6289=EDGE_LOOP ( 'NONE', ( #16238, #19392, #5277, #128, #14016 ) ) ;
#6294=DIRECTION ( 'NONE',  ( -1.000000000000000000, -0.000000000000000000, -0.000000000000000000 ) ) ;
#6316=ORIENTED_EDGE ( 'NONE', *, *, #18246, .F. ) ;
#6330=AXIS2_PLACEMENT_3D ( 'NONE', #10151, #19097, #15866 ) ;
#6379=ADVANCED_FACE ( 'NONE', ( #10607 ), #9531, .F. ) ;
#6393=DIRECTION ( 'NONE',  ( 0.000000000000000000, 0.000000000000000000, 1.000000000000000000 ) ) ;
#6402=EDGE_CURVE ( 'NONE', #11751, #9977, #12181, .T. ) ;
#6435=EDGE_CURVE ( 'NONE', #17858, #6216, #12469, .T. ) ;
#6473=ORIENTED_EDGE ( 'NONE', *, *, #1969, .T. ) ;
#6494=EDGE_CURVE ( 'NONE', #15771, #17858, #718, .T. ) ;
#6512=DIRECTION ( 'NONE',  ( 0.000000000000000000, 0.000000000000000000, -1.000000000000000000 ) ) ;
#6516=CARTESIAN_POINT ( 'NONE',  ( 3.099999999999998757, 0.000000000000000000, -1.600000000000000311 ) ) ;
#6522=ADVANCED_FACE ( 'NONE', ( #3938 ), #18752, .T. ) ;
#6527=CARTESIAN_POINT ( 'NONE',  ( 0.000000000000000000, -1.478016689125442706, 1.843143693225357538E-15 ) ) ;
#6549=AXIS2_PLACEMENT_3D ( 'NONE', #15498, #6585, #12264 ) ;
#6560=CARTESIAN_POINT ( 'NONE',  ( 0.000000000000000000, 0.000000000000000000, 0.000000000000000000 ) ) ;
#6582=CARTESIAN_POINT ( 'NONE',  ( 1.300000000000000044, -0.7390083445627200209, 1.280000000000001137 ) ) ;
#6585=DIRECTION ( 'NONE',  ( 0.000000000000000000, 0.8660254037844379305, -0.5000000000000014433 ) ) ;
#6599=ORIENTED_EDGE ( 'NONE', *, *, #4533, .T. ) ;
#6603=VECTOR ( 'NONE', #11962, 1000.000000000000114 ) ;
#6627=VECTOR ( 'NONE', #10753, 1000.000000000000000 ) ;
#6657=ADVANCED_BREP_SHAPE_REPRESENTATION ( '', ( #10426, #1791 ), #1419 ) ;
#6679=LINE ( 'NONE', #8058, #7890 ) ;
#6680=PLANE ( 'NONE',  #6549 ) ;
#6735=CARTESIAN_POINT ( 'NONE',  ( 11.00000000000000355, 0.000000000000000000, 1.219500000000000028 ) ) ;
#6807=DIRECTION ( 'NONE',  ( 0.000000000000000000, 0.000000000000000000, 1.000000000000000000 ) ) ;
#6845=EDGE_CURVE ( 'NONE', #834, #17858, #10966, .T. ) ;
#6864=VERTEX_POINT ( 'NONE', #18259 ) ;
#6869=DIRECTION ( 'NONE',  ( 0.000000000000000000, -1.000000000000000000, 1.320393690296331133E-15 ) ) ;
#6902=DIRECTION ( 'NONE',  ( 0.000000000000000000, -1.224646799147353207E-16, 1.000000000000000000 ) ) ;
#6921=CYLINDRICAL_SURFACE ( 'NONE', #10953, 1.500000000000000222 ) ;
#6946=VERTEX_POINT ( 'NONE', #13626 ) ;
#6962=ORIENTED_EDGE ( 'NONE', *, *, #7698, .T. ) ;
#6975=DIRECTION ( 'NONE',  ( -1.000000000000000000, -0.000000000000000000, -0.000000000000000000 ) ) ;
#7013=LINE ( 'NONE', #9668, #16917 ) ;
#7035=DIRECTION ( 'NONE',  ( -0.000000000000000000, 0.8660254037844391517, 0.4999999999999991118 ) ) ;
#7049=CARTESIAN_POINT ( 'NONE',  ( 0.1499999999999973577, 0.000000000000000000, 0.000000000000000000 ) ) ;
#7063=ORIENTED_EDGE ( 'NONE', *, *, #16757, .F. ) ;
#7076=EDGE_CURVE ( 'NONE', #15771, #13286, #11789, .T. ) ;
#7102=( NAMED_UNIT ( * ) PLANE_ANGLE_UNIT ( ) SI_UNIT ( $, .RADIAN. ) );
#7105=EDGE_CURVE ( 'NONE', #262, #11814, #2838, .T. ) ;
#7108=EDGE_CURVE ( 'NONE', #14101, #14697, #1615, .T. ) ;
#7133=VERTEX_POINT ( 'NONE', #13361 ) ;
#7171=VECTOR ( 'NONE', #973, 1000.000000000000000 ) ;
#7215=ADVANCED_FACE ( 'NONE', ( #7482, #18282 ), #5919, .T. ) ;
#7244=EDGE_CURVE ( 'NONE', #6946, #10557, #14111, .T. ) ;
#7246=CARTESIAN_POINT ( 'NONE',  ( 0.000000000000000000, -0.7390083445627200209, 1.280000000000001137 ) ) ;
#7271=DIRECTION ( 'NONE',  ( 0.000000000000000000, 0.000000000000000000, 1.000000000000000000 ) ) ;
#7392=PRODUCT_DEFINITION_SHAPE ( 'NONE', 'NONE',  #12552 ) ;
#7414=ADVANCED_FACE ( 'NONE', ( #4950 ), #10906, .F. ) ;
#7436=APPLICATION_CONTEXT ( 'automotive_design' ) ;
#7468=CARTESIAN_POINT ( 'NONE',  ( 1.300000000000000044, 1.478016689125442484, -1.626303258728256651E-15 ) ) ;
#7473=AXIS2_PLACEMENT_3D ( 'NONE', #7481, #17679, #1318 ) ;
#7481=CARTESIAN_POINT ( 'NONE',  ( 10.71950000000001424, 0.000000000000000000, 0.000000000000000000 ) ) ;
#7482=FACE_BOUND ( 'NONE', #4214, .T. ) ;
#7497=VECTOR ( 'NONE', #12578, 1000.000000000000227 ) ;
#7538=DIRECTION ( 'NONE',  ( 1.000000000000000000, 0.000000000000000000, 0.000000000000000000 ) ) ;
#7542=ORIENTED_EDGE ( 'NONE', *, *, #16757, .T. ) ;
#7548=EDGE_LOOP ( 'NONE', ( #12247, #18848, #1610, #13815 ) ) ;
#7566=EDGE_CURVE ( 'NONE', #12231, #9848, #9997, .T. ) ;
#7576=EDGE_CURVE ( 'NONE', #16562, #10557, #9437, .T. ) ;
#7588=CARTESIAN_POINT ( 'NONE',  ( 0.1499999999999973577, 0.000000000000000000, 0.000000000000000000 ) ) ;
#7591=DIRECTION ( 'NONE',  ( -1.000000000000000000, -0.000000000000000000, -0.000000000000000000 ) ) ;
#7646=DIRECTION ( 'NONE',  ( 1.000000000000000000, 0.000000000000000000, 0.000000000000000000 ) ) ;
#7679=ORIENTED_EDGE ( 'NONE', *, *, #13702, .T. ) ;
#7682=EDGE_LOOP ( 'NONE', ( #15955, #13281, #11797, #6473, #12625 ) ) ;
#7683=DIRECTION ( 'NONE',  ( 0.000000000000000000, -1.026972870230479989E-15, -1.000000000000000000 ) ) ;
#7698=EDGE_CURVE ( 'NONE', #11751, #834, #8188, .T. ) ;
#7728=CARTESIAN_POINT ( 'NONE',  ( 1.300000000000000044, 0.000000000000000000, 0.000000000000000000 ) ) ;
#7762=( LENGTH_UNIT ( ) NAMED_UNIT ( * ) SI_UNIT ( .MILLI., .METRE. ) );
#7780=ORIENTED_EDGE ( 'NONE', *, *, #6402, .F. ) ;
#7825=AXIS2_PLACEMENT_3D ( 'NONE', #12429, #15569, #8225 ) ;
#7839=AXIS2_PLACEMENT_3D ( 'NONE', #9904, #806, #11371 ) ;
#7855=ORIENTED_EDGE ( 'NONE', *, *, #965, .F. ) ;
#7864=CARTESIAN_POINT ( 'NONE',  ( 1.300000000000000044, 0.000000000000000000, 0.000000000000000000 ) ) ;
#7890=VECTOR ( 'NONE', #3439, 1000.000000000000000 ) ;
#7917=FACE_OUTER_BOUND ( 'NONE', #1015, .T. ) ;
#7930=ORIENTED_EDGE ( 'NONE', *, *, #6435, .F. ) ;
#7932=EDGE_CURVE ( 'NONE', #9301, #13286, #503, .T. ) ;
#8001=CARTESIAN_POINT ( 'NONE',  ( -31.74999999999995737, 0.000000000000000000, 0.000000000000000000 ) ) ;
#8034=ADVANCED_FACE ( 'NONE', ( #6267 ), #15188, .F. ) ;
#8058=CARTESIAN_POINT ( 'NONE',  ( 0.000000000000000000, -0.7390083445627200209, 1.280000000000001137 ) ) ;
#8070=EDGE_CURVE ( 'NONE', #9848, #2631, #17413, .T. ) ;
#8120=DIRECTION ( 'NONE',  ( 0.000000000000000000, 0.000000000000000000, 1.000000000000000000 ) ) ;
#8175=ADVANCED_FACE ( 'NONE', ( #14280 ), #8586, .F. ) ;
#8177=DIRECTION ( 'NONE',  ( 1.000000000000000000, 0.000000000000000000, 0.000000000000000000 ) ) ;
#8188=CIRCLE ( 'NONE', #17262, 1.280000000000000027 ) ;
#8191=ADVANCED_FACE ( 'NONE', ( #14862 ), #10339, .T. ) ;
#8222=DIRECTION ( 'NONE',  ( -1.000000000000000000, -0.000000000000000000, -0.000000000000000000 ) ) ;
#8225=DIRECTION ( 'NONE',  ( 0.000000000000000000, 0.000000000000000000, 1.000000000000000000 ) ) ;
#8279=VECTOR ( 'NONE', #7591, 1000.000000000000000 ) ;
#8317=EDGE_LOOP ( 'NONE', ( #14490, #10969, #4318, #5380 ) ) ;
#8354=CARTESIAN_POINT ( 'NONE',  ( 1.300000000000000044, 1.478016689125442484, -1.626303258728256651E-15 ) ) ;
#8355=ORIENTED_EDGE ( 'NONE', *, *, #4473, .F. ) ;
#8365=PLANE ( 'NONE',  #8642 ) ;
#8380=CARTESIAN_POINT ( 'NONE',  ( -31.74999999999995737, 0.000000000000000000, 2.750000000000000000 ) ) ;
#8397=CARTESIAN_POINT ( 'NONE',  ( 0.000000000000000000, 1.478016689125442484, -1.626303258728256651E-15 ) ) ;
#8458=VERTEX_POINT ( 'NONE', #13877 ) ;
#8465=VECTOR ( 'NONE', #10314, 1000.000000000000000 ) ;
#8488=DIRECTION ( 'NONE',  ( -1.000000000000000000, -0.000000000000000000, -0.000000000000000000 ) ) ;
#8490=VECTOR ( 'NONE', #14922, 1000.000000000000000 ) ;
#8522=SHAPE_REPRESENTATION ( 'socket head cap screw_iso_ISO 4762 M3 x 8 - 8N', ( #1791 ), #1419 ) ;
#8538=ORIENTED_EDGE ( 'NONE', *, *, #4989, .T. ) ;
#8586=PLANE ( 'NONE',  #13183 ) ;
#8590=ORIENTED_EDGE ( 'NONE', *, *, #5392, .F. ) ;
#8615=AXIS2_PLACEMENT_3D ( 'NONE', #1644, #15357, #12210 ) ;
#8632=ORIENTED_EDGE ( 'NONE', *, *, #5937, .T. ) ;
#8642=AXIS2_PLACEMENT_3D ( 'NONE', #17572, #4149, #13042 ) ;
#8653=CARTESIAN_POINT ( 'NONE',  ( 1.300000000000000044, 1.108512516844080364, -0.6400000000000017897 ) ) ;
#8689=ORIENTED_EDGE ( 'NONE', *, *, #16826, .T. ) ;
#8755=EDGE_CURVE ( 'NONE', #9977, #2631, #6099, .T. ) ;
#8776=AXIS2_PLACEMENT_3D ( 'NONE', #13753, #3072, #16805 ) ;
#8901=DIRECTION ( 'NONE',  ( 1.000000000000000000, 0.000000000000000000, 0.000000000000000000 ) ) ;
#8934=CARTESIAN_POINT ( 'NONE',  ( 1.300000000000000044, 1.567547902908612085E-16, -1.280000000000000027 ) ) ;
#8955=PRODUCT ( 'socket head cap screw_iso_ISO 4762 M3 x 8 - 8N', 'socket head cap screw_iso_ISO 4762 M3 x 8 - 8N', '', ( #14620 ) ) ;
#8960=FILL_AREA_STYLE_COLOUR ( '', #16764 ) ;
#8999=CARTESIAN_POINT ( 'NONE',  ( 1.300000000000000044, -0.7390083445627200209, 1.280000000000001137 ) ) ;
#9004=ADVANCED_FACE ( 'NONE', ( #4931 ), #2827, .T. ) ;
#9029=AXIS2_PLACEMENT_3D ( 'NONE', #18985, #12896, #5457 ) ;
#9069=CARTESIAN_POINT ( 'NONE',  ( 10.71950000000001424, 0.000000000000000000, 0.000000000000000000 ) ) ;
#9081=AXIS2_PLACEMENT_3D ( 'NONE', #1977, #6294, #3724 ) ;
#9096=ORIENTED_EDGE ( 'NONE', *, *, #10373, .T. ) ;
#9104=LINE ( 'NONE', #282, #11904 ) ;
#9107=ORIENTED_EDGE ( 'NONE', *, *, #4989, .F. ) ;
#9124=LINE ( 'NONE', #5894, #6603 ) ;
#9195=DIRECTION ( 'NONE',  ( -1.000000000000000000, -0.000000000000000000, -0.000000000000000000 ) ) ;
#9220=SURFACE_SIDE_STYLE ('',( #1875 ) ) ;
#9301=VERTEX_POINT ( 'NONE', #7246 ) ;
#9310=LINE ( 'NONE', #10874, #12207 ) ;
#9314=LINE ( 'NONE', #6582, #10317 ) ;
#9316=PRESENTATION_STYLE_ASSIGNMENT (( #15211 ) ) ;
#9335=CARTESIAN_POINT ( 'NONE',  ( 3.099999999999998757, 0.000000000000000000, 0.000000000000000000 ) ) ;
#9336=CONICAL_SURFACE ( 'NONE', #12769, 1.280000000000000027, 1.047197551196593857 ) ;
#9340=CARTESIAN_POINT ( 'NONE',  ( 3.000000000000002665, 0.000000000000000000, 2.750000000000000000 ) ) ;
#9359=CARTESIAN_POINT ( 'NONE',  ( 10.71950000000001424, 1.836970198721030181E-16, -1.500000000000000222 ) ) ;
#9380=ORIENTED_EDGE ( 'NONE', *, *, #1969, .F. ) ;
#9381=DIRECTION ( 'NONE',  ( -1.000000000000000000, -0.000000000000000000, -0.000000000000000000 ) ) ;
#9388=EDGE_CURVE ( 'NONE', #11814, #262, #9407, .T. ) ;
#9391=EDGE_CURVE ( 'NONE', #834, #6216, #9104, .T. ) ;
#9407=CIRCLE ( 'NONE', #14099, 2.750000000000000000 ) ;
#9437=CIRCLE ( 'NONE', #15697, 1.600000000000000311 ) ;
#9488=PLANE ( 'NONE',  #13804 ) ;
#9531=PLANE ( 'NONE',  #14371 ) ;
#9536=CARTESIAN_POINT ( 'NONE',  ( 0.000000000000000000, 0.7390083445627193548, -1.280000000000000693 ) ) ;
#9542=MECHANICAL_DESIGN_GEOMETRIC_PRESENTATION_REPRESENTATION('',(#15815),#3601);
#9550=DIRECTION ( 'NONE',  ( -1.000000000000000000, -0.000000000000000000, -0.000000000000000000 ) ) ;
#9561=ORIENTED_EDGE ( 'NONE', *, *, #7932, .T. ) ;
#9577=DIRECTION ( 'NONE',  ( 1.000000000000000000, 0.000000000000000000, 0.000000000000000000 ) ) ;
#9593=CARTESIAN_POINT ( 'NONE',  ( 10.71950000000001424, 0.000000000000000000, 1.500000000000000222 ) ) ;
#9596=ORIENTED_EDGE ( 'NONE', *, *, #2905, .T. ) ;
#9634=ADVANCED_FACE ( 'NONE', ( #4809, #570 ), #9488, .T. ) ;
#9665=ORIENTED_EDGE ( 'NONE', *, *, #19333, .F. ) ;
#9668=CARTESIAN_POINT ( 'NONE',  ( 1.300000000000000044, 0.7390083445627224634, 1.279999999999999138 ) ) ;
#9681=ORIENTED_EDGE ( 'NONE', *, *, #19333, .T. ) ;
#9725=ADVANCED_FACE ( 'NONE', ( #13082 ), #5459, .F. ) ;
#9798=ORIENTED_EDGE ( 'NONE', *, *, #8070, .T. ) ;
#9848=VERTEX_POINT ( 'NONE', #8397 ) ;
#9853=DIRECTION ( 'NONE',  ( 0.000000000000000000, 1.000000000000000000, -1.320393690296331133E-15 ) ) ;
#9867=ORIENTED_EDGE ( 'NONE', *, *, #7576, .T. ) ;
#9882=CARTESIAN_POINT ( 'NONE',  ( 11.00000000000000355, 1.493456771560197319E-16, -1.219500000000000028 ) ) ;
#9904=CARTESIAN_POINT ( 'NONE',  ( 11.00000000000000355, 1.219500000000000028, 0.000000000000000000 ) ) ;
#9942=CARTESIAN_POINT ( 'NONE',  ( 0.000000000000000000, -0.7390083445627225744, -1.279999999999999138 ) ) ;
#9961=ORIENTED_EDGE ( 'NONE', *, *, #7576, .F. ) ;
#9968=( NAMED_UNIT ( * ) SI_UNIT ( $, .STERADIAN. ) SOLID_ANGLE_UNIT ( ) );
#9977=VERTEX_POINT ( 'NONE', #13189 ) ;
#9997=LINE ( 'NONE', #16087, #16635 ) ;
#10013=DIRECTION ( 'NONE',  ( -1.000000000000000000, -0.000000000000000000, -0.000000000000000000 ) ) ;
#10032=SURFACE_STYLE_USAGE ( .BOTH. , #16415 ) ;
#10114=DIRECTION ( 'NONE',  ( 0.000000000000000000, 0.000000000000000000, 1.000000000000000000 ) ) ;
#10137=AXIS2_PLACEMENT_3D ( 'NONE', #19253, #12182, #18181 ) ;
#10151=CARTESIAN_POINT ( 'NONE',  ( 1.300000000000000044, 1.478016689125442484, -1.626303258728256651E-15 ) ) ;
#10168=ORIENTED_EDGE ( 'NONE', *, *, #15836, .F. ) ;
#10200=DIRECTION ( 'NONE',  ( 1.000000000000000000, 0.000000000000000000, 0.000000000000000000 ) ) ;
#10213=CIRCLE ( 'NONE', #11786, 1.600000000000000311 ) ;
#10258=EDGE_LOOP ( 'NONE', ( #15480, #13709, #14792 ) ) ;
#10287=CARTESIAN_POINT ( 'NONE',  ( 2.039008344562727615, -1.214068345727601445E-18, 0.000000000000000000 ) ) ;
#10314=DIRECTION ( 'NONE',  ( -1.000000000000000000, -0.000000000000000000, -0.000000000000000000 ) ) ;
#10317=VECTOR ( 'NONE', #3437, 1000.000000000000000 ) ;
#10323=( NAMED_UNIT ( * ) SI_UNIT ( $, .STERADIAN. ) SOLID_ANGLE_UNIT ( ) );
#10337=CARTESIAN_POINT ( 'NONE',  ( 11.00000000000000355, 0.000000000000000000, 1.219500000000000028 ) ) ;
#10339=CYLINDRICAL_SURFACE ( 'NONE', #11311, 1.500000000000000222 ) ;
#10373=EDGE_CURVE ( 'NONE', #9301, #15994, #6679, .T. ) ;
#10390=ORIENTED_EDGE ( 'NONE', *, *, #13586, .T. ) ;
#10410=CARTESIAN_POINT ( 'NONE',  ( 1.300000000000000044, -0.7390083445627225744, -1.279999999999999138 ) ) ;
#10426=MANIFOLD_SOLID_BREP ( 'Hex', #5062 ) ;
#10492=SHAPE_DEFINITION_REPRESENTATION ( #7392, #8522 ) ;
#10493=CARTESIAN_POINT ( 'NONE',  ( 1.300000000000000044, 0.7390083445627193548, -1.280000000000000693 ) ) ;
#10494=FACE_OUTER_BOUND ( 'NONE', #10606, .T. ) ;
#10543=ORIENTED_EDGE ( 'NONE', *, *, #6435, .T. ) ;
#10557=VERTEX_POINT ( 'NONE', #2534 ) ;
#10591=CIRCLE ( 'NONE', #9029, 1.280000000000000027 ) ;
#10602=CIRCLE ( 'NONE', #16883, 1.280000000000000027 ) ;
#10606=EDGE_LOOP ( 'NONE', ( #1748, #3872, #11720, #19121 ) ) ;
#10607=FACE_OUTER_BOUND ( 'NONE', #6289, .T. ) ;
#10654=CARTESIAN_POINT ( 'NONE',  ( 11.00000000000000355, 0.000000000000000000, 0.000000000000000000 ) ) ;
#10744=ORIENTED_EDGE ( 'NONE', *, *, #12432, .T. ) ;
#10750=ORIENTED_EDGE ( 'NONE', *, *, #867, .F. ) ;
#10753=DIRECTION ( 'NONE',  ( 0.000000000000000000, -1.000000000000000000, 1.026972870230479989E-15 ) ) ;
#10807=DIRECTION ( 'NONE',  ( 0.000000000000000000, 0.000000000000000000, -1.000000000000000000 ) ) ;
#10868=EDGE_LOOP ( 'NONE', ( #7855, #5219, #2606, #9107 ) ) ;
#10874=CARTESIAN_POINT ( 'NONE',  ( 0.000000000000000000, -1.478016689125442706, 1.843143693225357538E-15 ) ) ;
#10906=PLANE ( 'NONE',  #14426 ) ;
#10938=ORIENTED_EDGE ( 'NONE', *, *, #7698, .F. ) ;
#10946=ORIENTED_EDGE ( 'NONE', *, *, #5431, .T. ) ;
#10953=AXIS2_PLACEMENT_3D ( 'NONE', #3602, #8488, #8120 ) ;
#10955=AXIS2_PLACEMENT_3D ( 'NONE', #9069, #4668, #15056 ) ;
#10966=CIRCLE ( 'NONE', #1277, 1.280000000000000027 ) ;
#10969=ORIENTED_EDGE ( 'NONE', *, *, #5201, .T. ) ;
#11043=VERTEX_POINT ( 'NONE', #9593 ) ;
#11083=ORIENTED_EDGE ( 'NONE', *, *, #4635, .T. ) ;
#11142=DIRECTION ( 'NONE',  ( -0.000000000000000000, 0.000000000000000000, 1.000000000000000000 ) ) ;
#11169=DIRECTION ( 'NONE',  ( -1.000000000000000000, -0.000000000000000000, -0.000000000000000000 ) ) ;
#11180=ADVANCED_FACE ( 'NONE', ( #5667 ), #11824, .T. ) ;
#11212=VERTEX_POINT ( 'NONE', #14582 ) ;
#11244=CARTESIAN_POINT ( 'NONE',  ( 1.300000000000000044, -1.478016689125442706, 1.843143693225357538E-15 ) ) ;
#11277=AXIS2_PLACEMENT_3D ( 'NONE', #16017, #10013, #1199 ) ;
#11311=AXIS2_PLACEMENT_3D ( 'NONE', #18005, #16229, #16136 ) ;
#11371=DIRECTION ( 'NONE',  ( 0.000000000000000000, 0.000000000000000000, -1.000000000000000000 ) ) ;
#11394=LINE ( 'NONE', #17388, #16243 ) ;
#11461=PLANE ( 'NONE',  #1560 ) ;
#11491=CARTESIAN_POINT ( 'NONE',  ( 0.1499999999999973577, 0.000000000000000000, 0.000000000000000000 ) ) ;
#11547=ORIENTED_EDGE ( 'NONE', *, *, #6845, .F. ) ;
#11553=VECTOR ( 'NONE', #18573, 1000.000000000000114 ) ;
#11608=FACE_OUTER_BOUND ( 'NONE', #1030, .T. ) ;
#11610=FACE_OUTER_BOUND ( 'NONE', #5636, .T. ) ;
#11624=ORIENTED_EDGE ( 'NONE', *, *, #3524, .T. ) ;
#11720=ORIENTED_EDGE ( 'NONE', *, *, #12958, .F. ) ;
#11751=VERTEX_POINT ( 'NONE', #8653 ) ;
#11786=AXIS2_PLACEMENT_3D ( 'NONE', #14699, #5782, #11843 ) ;
#11789=LINE ( 'NONE', #17780, #8465 ) ;
#11797=ORIENTED_EDGE ( 'NONE', *, *, #6845, .T. ) ;
#11814=VERTEX_POINT ( 'NONE', #12870 ) ;
#11824=PLANE ( 'NONE',  #6330 ) ;
#11836=DIRECTION ( 'NONE',  ( 0.000000000000000000, -1.000000000000000000, 1.026972870230479989E-15 ) ) ;
#11843=DIRECTION ( 'NONE',  ( 0.000000000000000000, 0.000000000000000000, -1.000000000000000000 ) ) ;
#11853=ORIENTED_EDGE ( 'NONE', *, *, #5674, .T. ) ;
#11875=VECTOR ( 'NONE', #2731, 1000.000000000000000 ) ;
#11889=CARTESIAN_POINT ( 'NONE',  ( 3.000000000000000888, 2.750000000000000000, 0.000000000000000000 ) ) ;
#11904=VECTOR ( 'NONE', #11836, 1000.000000000000000 ) ;
#11962=DIRECTION ( 'NONE',  ( 0.000000000000000000, -0.5000000000000009992, -0.8660254037844380415 ) ) ;
#12003=LINE ( 'NONE', #10337, #17495 ) ;
#12032=VECTOR ( 'NONE', #16404, 1000.000000000000000 ) ;
#12038=EDGE_CURVE ( 'NONE', #6946, #16414, #16258, .T. ) ;
#12039=CARTESIAN_POINT ( 'NONE',  ( 0.1499999999999973577, 0.000000000000000000, 0.000000000000000000 ) ) ;
#12083=CARTESIAN_POINT ( 'NONE',  ( 1.300000000000000044, 0.000000000000000000, 1.280000000000000027 ) ) ;
#12105=FACE_OUTER_BOUND ( 'NONE', #7682, .T. ) ;
#12133=CARTESIAN_POINT ( 'NONE',  ( 3.099999999999998757, 0.000000000000000000, 0.000000000000000000 ) ) ;
#12141=ORIENTED_EDGE ( 'NONE', *, *, #3310, .T. ) ;
#12181=LINE ( 'NONE', #3172, #7497 ) ;
#12182=DIRECTION ( 'NONE',  ( -1.000000000000000000, -0.000000000000000000, -0.000000000000000000 ) ) ;
#12207=VECTOR ( 'NONE', #688, 1000.000000000000114 ) ;
#12210=DIRECTION ( 'NONE',  ( 0.000000000000000000, 0.5000000000000009992, 0.8660254037844380415 ) ) ;
#12230=VECTOR ( 'NONE', #12289, 999.9999999999998863 ) ;
#12231=VERTEX_POINT ( 'NONE', #8354 ) ;
#12247=ORIENTED_EDGE ( 'NONE', *, *, #9388, .F. ) ;
#12264=DIRECTION ( 'NONE',  ( 0.000000000000000000, 0.5000000000000013323, 0.8660254037844378194 ) ) ;
#12289=DIRECTION ( 'NONE',  ( -0.5000000000000034417, 0.000000000000000000, 0.8660254037844367092 ) ) ;
#12366=ORIENTED_EDGE ( 'NONE', *, *, #5392, .T. ) ;
#12429=CARTESIAN_POINT ( 'NONE',  ( 1.300000000000000044, 0.000000000000000000, 0.000000000000000000 ) ) ;
#12432=EDGE_CURVE ( 'NONE', #4916, #7133, #9124, .T. ) ;
#12435=ORIENTED_EDGE ( 'NONE', *, *, #7244, .T. ) ;
#12469=LINE ( 'NONE', #18472, #11553 ) ;
#12472=DIRECTION ( 'NONE',  ( 0.000000000000000000, 0.000000000000000000, -1.000000000000000000 ) ) ;
#12480=EDGE_CURVE ( 'NONE', #11212, #18570, #15111, .T. ) ;
#12492=CONICAL_SURFACE ( 'NONE', #14669, 1.280000000000000027, 1.047197551196593857 ) ;
#12548=ORIENTED_EDGE ( 'NONE', *, *, #7076, .T. ) ;
#12552=PRODUCT_DEFINITION ( 'UNKNOWN', '', #484, #16890 ) ;
#12565=ORIENTED_EDGE ( 'NONE', *, *, #6402, .T. ) ;
#12576=DIRECTION ( 'NONE',  ( 0.000000000000000000, 0.000000000000000000, -1.000000000000000000 ) ) ;
#12577=ORIENTED_EDGE ( 'NONE', *, *, #4635, .F. ) ;
#12578=DIRECTION ( 'NONE',  ( 0.000000000000000000, -0.5000000000000013323, -0.8660254037844378194 ) ) ;
#12621=EDGE_CURVE ( 'NONE', #4916, #14697, #9314, .T. ) ;
#12625=ORIENTED_EDGE ( 'NONE', *, *, #1919, .T. ) ;
#12763=CARTESIAN_POINT ( 'NONE',  ( 1.300000000000000044, 0.7390083445627224634, 1.279999999999999138 ) ) ;
#12765=ORIENTED_EDGE ( 'NONE', *, *, #6494, .T. ) ;
#12769=AXIS2_PLACEMENT_3D ( 'NONE', #17910, #4481, #16427 ) ;
#12782=AXIS2_PLACEMENT_3D ( 'NONE', #14254, #919, #6902 ) ;
#12870=CARTESIAN_POINT ( 'NONE',  ( 0.1499999999999973577, 3.367778697655221012E-16, -2.750000000000000000 ) ) ;
#12896=DIRECTION ( 'NONE',  ( -1.000000000000000000, -0.000000000000000000, -0.000000000000000000 ) ) ;
#12942=DIRECTION ( 'NONE',  ( -1.000000000000000000, -0.000000000000000000, -0.000000000000000000 ) ) ;
#12958=EDGE_CURVE ( 'NONE', #11043, #2345, #14087, .T. ) ;
#12959=AXIS2_PLACEMENT_3D ( 'NONE', #8001, #9550, #6807 ) ;
#12983=TOROIDAL_SURFACE ( 'NONE', #13614, 1.600000000000000311, 0.1000000000000000056 ) ;
#13034=CARTESIAN_POINT ( 'NONE',  ( 1.300000000000000044, -1.478016689125442706, 1.843143693225357538E-15 ) ) ;
#13042=DIRECTION ( 'NONE',  ( 0.000000000000000000, 0.000000000000000000, -1.000000000000000000 ) ) ;
#13050=CARTESIAN_POINT ( 'NONE',  ( 3.000000000000002665, 0.000000000000000000, 0.000000000000000000 ) ) ;
#13082=FACE_OUTER_BOUND ( 'NONE', #96, .T. ) ;
#13093=EDGE_LOOP ( 'NONE', ( #9096, #12577, #95, #14868, #10390 ) ) ;
#13135=CARTESIAN_POINT ( 'NONE',  ( 3.000000000000000888, 0.000000000000000000, 0.000000000000000000 ) ) ;
#13150=CIRCLE ( 'NONE', #11277, 2.600000000000000089 ) ;
#13183=AXIS2_PLACEMENT_3D ( 'NONE', #14566, #3700, #1138 ) ;
#13189=CARTESIAN_POINT ( 'NONE',  ( 1.300000000000000044, 0.7390083445627193548, -1.280000000000000693 ) ) ;
#13208=ADVANCED_FACE ( 'NONE', ( #823 ), #541, .T. ) ;
#13209=EDGE_LOOP ( 'NONE', ( #16798, #8590, #9380 ) ) ;
#13242=LINE ( 'NONE', #8934, #18685 ) ;
#13281=ORIENTED_EDGE ( 'NONE', *, *, #18679, .T. ) ;
#13286=VERTEX_POINT ( 'NONE', #6527 ) ;
#13328=CARTESIAN_POINT ( 'NONE',  ( 1.300000000000000044, 1.478016689125442484, -1.626303258728256651E-15 ) ) ;
#13344=CONICAL_SURFACE ( 'NONE', #16163, 1.219500000000000028, 0.7853981633974680410 ) ;
#13361=CARTESIAN_POINT ( 'NONE',  ( 1.300000000000000044, -1.108512516844081475, 0.6400000000000016787 ) ) ;
#13367=ORIENTED_EDGE ( 'NONE', *, *, #18679, .F. ) ;
#13368=( LENGTH_UNIT ( ) NAMED_UNIT ( * ) SI_UNIT ( .MILLI., .METRE. ) );
#13453=DIRECTION ( 'NONE',  ( -1.000000000000000000, -0.000000000000000000, -0.000000000000000000 ) ) ;
#13485=AXIS2_PLACEMENT_3D ( 'NONE', #4899, #9577, #15571 ) ;
#13504=EDGE_CURVE ( 'NONE', #9977, #834, #15917, .T. ) ;
#13532=ORIENTED_EDGE ( 'NONE', *, *, #4473, .T. ) ;
#13554=LINE ( 'NONE', #16306, #18939 ) ;
#13586=EDGE_CURVE ( 'NONE', #4916, #9301, #13554, .T. ) ;
#13614=AXIS2_PLACEMENT_3D ( 'NONE', #9335, #15433, #12472 ) ;
#13626=CARTESIAN_POINT ( 'NONE',  ( 3.099999999999998757, 0.000000000000000000, 1.500000000000000222 ) ) ;
#13650=CARTESIAN_POINT ( 'NONE',  ( 1.300000000000000044, 0.7390083445627193548, -1.280000000000000693 ) ) ;
#13655=LINE ( 'NONE', #4464, #18926 ) ;
#13669=EDGE_CURVE ( 'NONE', #201, #6864, #18629, .T. ) ;
#13702=EDGE_CURVE ( 'NONE', #6216, #2004, #1409, .T. ) ;
#13709=ORIENTED_EDGE ( 'NONE', *, *, #12480, .F. ) ;
#13713=CARTESIAN_POINT ( 'NONE',  ( 0.000000000000000000, 0.000000000000000000, 0.000000000000000000 ) ) ;
#13727=DIRECTION ( 'NONE',  ( -1.000000000000000000, -0.000000000000000000, -0.000000000000000000 ) ) ;
#13735=CARTESIAN_POINT ( 'NONE',  ( 11.00000000000000355, 0.000000000000000000, 0.000000000000000000 ) ) ;
#13740=ORIENTED_EDGE ( 'NONE', *, *, #12480, .T. ) ;
#13743=TOROIDAL_SURFACE ( 'NONE', #3417, 1.600000000000000311, 0.1000000000000000056 ) ;
#13750=ADVANCED_FACE ( 'NONE', ( #5141 ), #12983, .F. ) ;
#13753=CARTESIAN_POINT ( 'NONE',  ( 3.099999999999998757, 1.959434878635765477E-16, 1.600000000000000311 ) ) ;
#13801=CARTESIAN_POINT ( 'NONE',  ( 3.000000000000002665, 0.000000000000000000, 0.000000000000000000 ) ) ;
#13804=AXIS2_PLACEMENT_3D ( 'NONE', #6560, #3609, #11142 ) ;
#13813=VECTOR ( 'NONE', #2164, 1000.000000000000114 ) ;
#13815=ORIENTED_EDGE ( 'NONE', *, *, #1150, .F. ) ;
#13877=CARTESIAN_POINT ( 'NONE',  ( 0.000000000000000000, 3.275930187719169848E-16, -2.600000000000000089 ) ) ;
#13882=ORIENTED_EDGE ( 'NONE', *, *, #7566, .T. ) ;
#14016=ORIENTED_EDGE ( 'NONE', *, *, #8755, .T. ) ;
#14087=CIRCLE ( 'NONE', #10955, 1.500000000000000222 ) ;
#14092=CARTESIAN_POINT ( 'NONE',  ( 0.000000000000000000, 0.7390083445627193548, -1.280000000000000693 ) ) ;
#14099=AXIS2_PLACEMENT_3D ( 'NONE', #12039, #7538, #6178 ) ;
#14101=VERTEX_POINT ( 'NONE', #10287 ) ;
#14111=CIRCLE ( 'NONE', #8776, 0.1000000000000000472 ) ;
#14121=ORIENTED_EDGE ( 'NONE', *, *, #259, .F. ) ;
#14166=DIRECTION ( 'NONE',  ( -1.000000000000000000, -0.000000000000000000, -0.000000000000000000 ) ) ;
#14242=DIRECTION ( 'NONE',  ( 0.000000000000000000, -1.000000000000000000, 0.000000000000000000 ) ) ;
#14254=CARTESIAN_POINT ( 'NONE',  ( 0.1499999999999973577, 3.184081677783118191E-16, -2.600000000000000089 ) ) ;
#14280=FACE_OUTER_BOUND ( 'NONE', #1800, .T. ) ;
#14289=ORIENTED_EDGE ( 'NONE', *, *, #1024, .T. ) ;
#14296=PLANE ( 'NONE',  #4383 ) ;
#14353=CIRCLE ( 'NONE', #7473, 1.500000000000000222 ) ;
#14371=AXIS2_PLACEMENT_3D ( 'NONE', #18279, #7683, #15523 ) ;
#14388=ORIENTED_EDGE ( 'NONE', *, *, #13669, .F. ) ;
#14393=VECTOR ( 'NONE', #9195, 1000.000000000000000 ) ;
#14414=FACE_OUTER_BOUND ( 'NONE', #13093, .T. ) ;
#14426=AXIS2_PLACEMENT_3D ( 'NONE', #15615, #8177, #6512 ) ;
#14490=ORIENTED_EDGE ( 'NONE', *, *, #12958, .T. ) ;
#14507=EDGE_CURVE ( 'NONE', #14697, #11212, #504, .T. ) ;
#14566=CARTESIAN_POINT ( 'NONE',  ( 1.300000000000000044, 1.478016689125442484, -1.626303258728256651E-15 ) ) ;
#14577=VERTEX_POINT ( 'NONE', #15462 ) ;
#14582=CARTESIAN_POINT ( 'NONE',  ( 1.300000000000000044, 1.108512516844082141, 0.6399999999999991251 ) ) ;
#14610=CARTESIAN_POINT ( 'NONE',  ( 1.300000000000000044, 1.478016689125442484, -1.626303258728256651E-15 ) ) ;
#14620=PRODUCT_CONTEXT ( 'NONE', #2679, 'mechanical' ) ;
#14663=DIRECTION ( 'NONE',  ( 0.000000000000000000, 0.000000000000000000, -1.000000000000000000 ) ) ;
#14664=CARTESIAN_POINT ( 'NONE',  ( 3.099999999999998757, 0.000000000000000000, 0.000000000000000000 ) ) ;
#14669=AXIS2_PLACEMENT_3D ( 'NONE', #17803, #2702, #4380 ) ;
#14685=DIRECTION ( 'NONE',  ( 0.000000000000000000, -0.5000000000000009992, -0.8660254037844380415 ) ) ;
#14697=VERTEX_POINT ( 'NONE', #17037 ) ;
#14699=CARTESIAN_POINT ( 'NONE',  ( 3.000000000000000888, 0.000000000000000000, 0.000000000000000000 ) ) ;
#14715=DIRECTION ( 'NONE',  ( -1.000000000000000000, -0.000000000000000000, -0.000000000000000000 ) ) ;
#14792=ORIENTED_EDGE ( 'NONE', *, *, #14507, .F. ) ;
#14827=DIRECTION ( 'NONE',  ( -0.5000000000000034417, 1.060575238724904696E-16, -0.8660254037844367092 ) ) ;
#14840=CARTESIAN_POINT ( 'NONE',  ( 0.1499999999999973577, 0.000000000000000000, 2.600000000000000089 ) ) ;
#14848=( LENGTH_UNIT ( ) NAMED_UNIT ( * ) SI_UNIT ( .MILLI., .METRE. ) );
#14862=FACE_OUTER_BOUND ( 'NONE', #8317, .T. ) ;
#14867=DIRECTION ( 'NONE',  ( 1.000000000000000000, 0.000000000000000000, 0.000000000000000000 ) ) ;
#14868=ORIENTED_EDGE ( 'NONE', *, *, #12621, .F. ) ;
#14922=DIRECTION ( 'NONE',  ( -1.000000000000000000, -0.000000000000000000, -0.000000000000000000 ) ) ;
#14930=ADVANCED_FACE ( 'NONE', ( #7917 ), #260, .T. ) ;
#14980=ORIENTED_EDGE ( 'NONE', *, *, #8755, .F. ) ;
#14994=CIRCLE ( 'NONE', #12782, 0.1499999999999999667 ) ;
#15036=CARTESIAN_POINT ( 'NONE',  ( 1.300000000000000044, 0.000000000000000000, 0.000000000000000000 ) ) ;
#15056=DIRECTION ( 'NONE',  ( 0.000000000000000000, 0.000000000000000000, 1.000000000000000000 ) ) ;
#15087=CARTESIAN_POINT ( 'NONE',  ( -31.74999999999995737, 0.000000000000000000, 1.500000000000000222 ) ) ;
#15111=LINE ( 'NONE', #13328, #2499 ) ;
#15124=PLANE ( 'NONE',  #4918 ) ;
#15130=DIRECTION ( 'NONE',  ( 0.000000000000000000, -0.4999999999999992784, 0.8660254037844390407 ) ) ;
#15167=VERTEX_POINT ( 'NONE', #18882 ) ;
#15176=DIRECTION ( 'NONE',  ( 0.000000000000000000, 0.000000000000000000, 1.000000000000000000 ) ) ;
#15188=PLANE ( 'NONE',  #13485 ) ;
#15211=SURFACE_STYLE_USAGE ( .BOTH. , #9220 ) ;
#15278=DIRECTION ( 'NONE',  ( -1.000000000000000000, -0.000000000000000000, -0.000000000000000000 ) ) ;
#15308=CARTESIAN_POINT ( 'NONE',  ( 11.00000000000000355, 0.000000000000000000, 0.000000000000000000 ) ) ;
#15357=DIRECTION ( 'NONE',  ( 0.000000000000000000, 0.8660254037844380415, -0.5000000000000009992 ) ) ;
#15433=DIRECTION ( 'NONE',  ( 1.000000000000000000, 0.000000000000000000, 0.000000000000000000 ) ) ;
#15462=CARTESIAN_POINT ( 'NONE',  ( 0.000000000000000000, 0.000000000000000000, 2.600000000000000089 ) ) ;
#15480=ORIENTED_EDGE ( 'NONE', *, *, #5527, .T. ) ;
#15498=CARTESIAN_POINT ( 'NONE',  ( 1.300000000000000044, 1.478016689125442484, -1.626303258728256651E-15 ) ) ;
#15523=DIRECTION ( 'NONE',  ( 0.000000000000000000, 1.000000000000000000, -1.026972870230479989E-15 ) ) ;
#15535=VERTEX_POINT ( 'NONE', #9340 ) ;
#15569=DIRECTION ( 'NONE',  ( -1.000000000000000000, -0.000000000000000000, -0.000000000000000000 ) ) ;
#15571=DIRECTION ( 'NONE',  ( 0.000000000000000000, 0.000000000000000000, -1.000000000000000000 ) ) ;
#15615=CARTESIAN_POINT ( 'NONE',  ( 1.300000000000000044, 1.478016689125442484, -1.626303258728256651E-15 ) ) ;
#15639=AXIS2_PLACEMENT_3D ( 'NONE', #18277, #613, #12576 ) ;
#15658=ORIENTED_EDGE ( 'NONE', *, *, #1039, .T. ) ;
#15697=AXIS2_PLACEMENT_3D ( 'NONE', #13135, #12942, #19231 ) ;
#15771=VERTEX_POINT ( 'NONE', #723 ) ;
#15812=FACE_OUTER_BOUND ( 'NONE', #4494, .T. ) ;
#15815=STYLED_ITEM ( 'NONE', ( #2888 ), #6657 ) ;
#15836=EDGE_CURVE ( 'NONE', #16414, #16562, #18385, .T. ) ;
#15866=DIRECTION ( 'NONE',  ( 0.000000000000000000, 0.4999999999999992228, -0.8660254037844390407 ) ) ;
#15876=LINE ( 'NONE', #4111, #7171 ) ;
#15917=LINE ( 'NONE', #13650, #3285 ) ;
#15928=ORIENTED_EDGE ( 'NONE', *, *, #867, .T. ) ;
#15951=ADVANCED_FACE ( 'NONE', ( #10494 ), #13344, .T. ) ;
#15955=ORIENTED_EDGE ( 'NONE', *, *, #7108, .F. ) ;
#15994=VERTEX_POINT ( 'NONE', #18363 ) ;
#16017=CARTESIAN_POINT ( 'NONE',  ( 0.000000000000000000, 0.000000000000000000, 0.000000000000000000 ) ) ;
#16084=ORIENTED_EDGE ( 'NONE', *, *, #3524, .F. ) ;
#16087=CARTESIAN_POINT ( 'NONE',  ( 1.300000000000000044, 1.478016689125442484, -1.626303258728256651E-15 ) ) ;
#16104=DIRECTION ( 'NONE',  ( 0.000000000000000000, 0.000000000000000000, 1.000000000000000000 ) ) ;
#16130=CARTESIAN_POINT ( 'NONE',  ( -31.74999999999995737, 0.000000000000000000, 0.000000000000000000 ) ) ;
#16136=DIRECTION ( 'NONE',  ( 0.000000000000000000, 0.000000000000000000, 1.000000000000000000 ) ) ;
#16157=ORIENTED_EDGE ( 'NONE', *, *, #10373, .F. ) ;
#16163=AXIS2_PLACEMENT_3D ( 'NONE', #13735, #118, #317 ) ;
#16185=CARTESIAN_POINT ( 'NONE',  ( 1.300000000000000044, 0.000000000000000000, 0.000000000000000000 ) ) ;
#16206=CARTESIAN_POINT ( 'NONE',  ( 1.300000000000000044, -0.7390083445627200209, 1.280000000000001137 ) ) ;
#16229=DIRECTION ( 'NONE',  ( -1.000000000000000000, -0.000000000000000000, -0.000000000000000000 ) ) ;
#16238=ORIENTED_EDGE ( 'NONE', *, *, #259, .T. ) ;
#16243=VECTOR ( 'NONE', #14166, 1000.000000000000000 ) ;
#16258=CIRCLE ( 'NONE', #15639, 1.500000000000000222 ) ;
#16306=CARTESIAN_POINT ( 'NONE',  ( 1.300000000000000044, -0.7390083445627200209, 1.280000000000001137 ) ) ;
#16361=FACE_OUTER_BOUND ( 'NONE', #3426, .T. ) ;
#16404=DIRECTION ( 'NONE',  ( -1.000000000000000000, -0.000000000000000000, -0.000000000000000000 ) ) ;
#16414=VERTEX_POINT ( 'NONE', #16431 ) ;
#16415=SURFACE_SIDE_STYLE ('',( #17596 ) ) ;
#16427=DIRECTION ( 'NONE',  ( 0.000000000000000000, 0.000000000000000000, 1.000000000000000000 ) ) ;
#16431=CARTESIAN_POINT ( 'NONE',  ( 3.099999999999998757, 1.836970198721030181E-16, -1.500000000000000222 ) ) ;
#16454=ORIENTED_EDGE ( 'NONE', *, *, #1919, .F. ) ;
#16497=UNCERTAINTY_MEASURE_WITH_UNIT (LENGTH_MEASURE( 1.000000000000000082E-05 ), #13368, 'distance_accuracy_value', 'NONE');
#16509=DIRECTION ( 'NONE',  ( 0.000000000000000000, 0.000000000000000000, 1.000000000000000000 ) ) ;
#16560=CARTESIAN_POINT ( 'NONE',  ( 1.300000000000000044, -1.108512516844082141, -0.6399999999999991251 ) ) ;
#16562=VERTEX_POINT ( 'NONE', #1932 ) ;
#16608=DIRECTION ( 'NONE',  ( 1.000000000000000000, 0.000000000000000000, 0.000000000000000000 ) ) ;
#16609=AXIS2_PLACEMENT_3D ( 'NONE', #10654, #9381, #5090 ) ;
#16617=ORIENTED_EDGE ( 'NONE', *, *, #2905, .F. ) ;
#16635=VECTOR ( 'NONE', #6975, 1000.000000000000000 ) ;
#16640=COLOUR_RGB ( '', 0.09019608, 0.27058824, 0.51372549) ;
#16684=FILL_AREA_STYLE ('',( #3351 ) ) ;
#16757=EDGE_CURVE ( 'NONE', #15535, #262, #2395, .T. ) ;
#16764=COLOUR_RGB ( '', 0.09019608, 0.27058824, 0.51372549) ;
#16798=ORIENTED_EDGE ( 'NONE', *, *, #6494, .F. ) ;
#16805=DIRECTION ( 'NONE',  ( 0.000000000000000000, 1.224646799147353207E-16, 1.000000000000000000 ) ) ;
#16826=EDGE_CURVE ( 'NONE', #9848, #15994, #13655, .T. ) ;
#16877=FACE_OUTER_BOUND ( 'NONE', #2945, .T. ) ;
#16883=AXIS2_PLACEMENT_3D ( 'NONE', #15036, #1206, #6393 ) ;
#16890=PRODUCT_DEFINITION_CONTEXT ( 'detailed design', #7436, 'design' ) ;
#16917=VECTOR ( 'NONE', #8222, 1000.000000000000000 ) ;
#16978=ORIENTED_EDGE ( 'NONE', *, *, #7244, .F. ) ;
#17037=CARTESIAN_POINT ( 'NONE',  ( 1.300000000000000044, 1.690103923579304181E-15, 1.280000000000000249 ) ) ;
#17084=ORIENTED_EDGE ( 'NONE', *, *, #5201, .F. ) ;
#17228=DIRECTION ( 'NONE',  ( -1.000000000000000000, -0.000000000000000000, -0.000000000000000000 ) ) ;
#17262=AXIS2_PLACEMENT_3D ( 'NONE', #16185, #14715, #7271 ) ;
#17321=LINE ( 'NONE', #3885, #2176 ) ;
#17388=CARTESIAN_POINT ( 'NONE',  ( -31.74999999999995737, 3.367778697655221012E-16, -2.750000000000000000 ) ) ;
#17413=LINE ( 'NONE', #18708, #2242 ) ;
#17444=DIRECTION ( 'NONE',  ( -1.000000000000000000, -0.000000000000000000, -0.000000000000000000 ) ) ;
#17485=ADVANCED_FACE ( 'NONE', ( #3831 ), #2048, .T. ) ;
#17495=VECTOR ( 'NONE', #4182, 1000.000000000000000 ) ;
#17572=CARTESIAN_POINT ( 'NONE',  ( 1.300000000000000044, 1.478016689125442484, -1.626303258728256651E-15 ) ) ;
#17596=SURFACE_STYLE_FILL_AREA ( #1327 ) ;
#17604=DIRECTION ( 'NONE',  ( 0.000000000000000000, 0.000000000000000000, 1.000000000000000000 ) ) ;
#17612=ORIENTED_EDGE ( 'NONE', *, *, #12432, .F. ) ;
#17679=DIRECTION ( 'NONE',  ( -1.000000000000000000, -0.000000000000000000, -0.000000000000000000 ) ) ;
#17743=ORIENTED_EDGE ( 'NONE', *, *, #5937, .F. ) ;
#17779=FACE_OUTER_BOUND ( 'NONE', #7548, .T. ) ;
#17780=CARTESIAN_POINT ( 'NONE',  ( 1.300000000000000044, -1.478016689125442706, 1.843143693225357538E-15 ) ) ;
#17803=CARTESIAN_POINT ( 'NONE',  ( 1.300000000000000044, 0.000000000000000000, 0.000000000000000000 ) ) ;
#17858=VERTEX_POINT ( 'NONE', #16560 ) ;
#17886=DIRECTION ( 'NONE',  ( 0.000000000000000000, 0.000000000000000000, -1.000000000000000000 ) ) ;
#17887=DIRECTION ( 'NONE',  ( 1.000000000000000000, 0.000000000000000000, 0.000000000000000000 ) ) ;
#17896=( GEOMETRIC_REPRESENTATION_CONTEXT ( 3 ) GLOBAL_UNCERTAINTY_ASSIGNED_CONTEXT ( ( #3568 ) ) GLOBAL_UNIT_ASSIGNED_CONTEXT ( ( #7762, #306, #9968 ) ) REPRESENTATION_CONTEXT ( 'NONE', 'WORKASPACE' ) );
#17910=CARTESIAN_POINT ( 'NONE',  ( 1.300000000000000044, 0.000000000000000000, 0.000000000000000000 ) ) ;
#17967=ORIENTED_EDGE ( 'NONE', *, *, #7105, .T. ) ;
#18005=CARTESIAN_POINT ( 'NONE',  ( -31.74999999999995737, 0.000000000000000000, 0.000000000000000000 ) ) ;
#18068=DIRECTION ( 'NONE',  ( 0.000000000000000000, 0.000000000000000000, -1.000000000000000000 ) ) ;
#18181=DIRECTION ( 'NONE',  ( 0.000000000000000000, 0.000000000000000000, 1.000000000000000000 ) ) ;
#18193=AXIS2_PLACEMENT_3D ( 'NONE', #11889, #16608, #10807 ) ;
#18246=EDGE_CURVE ( 'NONE', #16414, #6946, #1758, .T. ) ;
#18259=CARTESIAN_POINT ( 'NONE',  ( 11.00000000000000355, 1.665213485140613626E-16, -1.219500000000000028 ) ) ;
#18262=CARTESIAN_POINT ( 'NONE',  ( 0.000000000000000000, -0.7390083445627200209, 1.280000000000001137 ) ) ;
#18277=CARTESIAN_POINT ( 'NONE',  ( 3.099999999999998757, 0.000000000000000000, 0.000000000000000000 ) ) ;
#18279=CARTESIAN_POINT ( 'NONE',  ( 1.300000000000000044, 0.7390083445627193548, -1.280000000000000693 ) ) ;
#18282=FACE_OUTER_BOUND ( 'NONE', #5190, .T. ) ;
#18315=ORIENTED_EDGE ( 'NONE', *, *, #15836, .T. ) ;
#18363=CARTESIAN_POINT ( 'NONE',  ( 0.000000000000000000, 0.7390083445627224634, 1.279999999999999138 ) ) ;
#18385=CIRCLE ( 'NONE', #5840, 0.1000000000000000472 ) ;
#18444=ORIENTED_EDGE ( 'NONE', *, *, #12621, .T. ) ;
#18472=CARTESIAN_POINT ( 'NONE',  ( 1.300000000000000044, -1.478016689125442706, 1.843143693225357538E-15 ) ) ;
#18496=CARTESIAN_POINT ( 'NONE',  ( 1.300000000000000044, -1.314525273895014473E-15, -1.280000000000000027 ) ) ;
#18530=ADVANCED_FACE ( 'NONE', ( #15812 ), #8365, .F. ) ;
#18536=ORIENTED_EDGE ( 'NONE', *, *, #3289, .T. ) ;
#18570=VERTEX_POINT ( 'NONE', #12763 ) ;
#18573=DIRECTION ( 'NONE',  ( 0.000000000000000000, 0.4999999999999991673, -0.8660254037844391517 ) ) ;
#18608=EDGE_LOOP ( 'NONE', ( #16617, #1105, #12765, #10543, #7679 ) ) ;
#18629=CIRCLE ( 'NONE', #10137, 1.219500000000000028 ) ;
#18679=EDGE_CURVE ( 'NONE', #14101, #834, #13242, .T. ) ;
#18685=VECTOR ( 'NONE', #14827, 999.9999999999998863 ) ;
#18708=CARTESIAN_POINT ( 'NONE',  ( 0.000000000000000000, 1.478016689125442484, -1.626303258728256651E-15 ) ) ;
#18742=ADVANCED_FACE ( 'NONE', ( #4442 ), #15124, .F. ) ;
#18752=PLANE ( 'NONE',  #7839 ) ;
#18792=AXIS2_PLACEMENT_3D ( 'NONE', #13050, #18954, #16104 ) ;
#18848=ORIENTED_EDGE ( 'NONE', *, *, #965, .T. ) ;
#18882=CARTESIAN_POINT ( 'NONE',  ( 3.000000000000002665, 3.367778697655221012E-16, -2.750000000000000000 ) ) ;
#18926=VECTOR ( 'NONE', #238, 1000.000000000000000 ) ;
#18935=DIRECTION ( 'NONE',  ( 0.000000000000000000, 0.4999999999999991673, -0.8660254037844391517 ) ) ;
#18939=VECTOR ( 'NONE', #37, 1000.000000000000000 ) ;
#18954=DIRECTION ( 'NONE',  ( -1.000000000000000000, -0.000000000000000000, -0.000000000000000000 ) ) ;
#18985=CARTESIAN_POINT ( 'NONE',  ( 1.300000000000000044, 0.000000000000000000, 0.000000000000000000 ) ) ;
#19019=ORIENTED_EDGE ( 'NONE', *, *, #7932, .F. ) ;
#19063=ORIENTED_EDGE ( 'NONE', *, *, #9388, .T. ) ;
#19097=DIRECTION ( 'NONE',  ( 0.000000000000000000, -0.8660254037844391517, -0.4999999999999992784 ) ) ;
#19121=ORIENTED_EDGE ( 'NONE', *, *, #5674, .F. ) ;
#19124=LINE ( 'NONE', #14610, #2480 ) ;
#19231=DIRECTION ( 'NONE',  ( 0.000000000000000000, 0.000000000000000000, -1.000000000000000000 ) ) ;
#19253=CARTESIAN_POINT ( 'NONE',  ( 11.00000000000000355, 0.000000000000000000, 0.000000000000000000 ) ) ;
#19333=EDGE_CURVE ( 'NONE', #10557, #16562, #10213, .T. ) ;
#19352=DIRECTION ( 'NONE',  ( 0.000000000000000000, -1.000000000000000000, 0.000000000000000000 ) ) ;
#19392=ORIENTED_EDGE ( 'NONE', *, *, #13702, .F. ) ;
ENDSEC;
END-ISO-10303-21;
